ISO-10303-21;
HEADER;
/* Generated by software containing ST-Developer
 * from STEP Tools, Inc. (www.steptools.com) 
 */

FILE_DESCRIPTION(
/* description */ ('CAx-IF Rec.Pracs.---Representation and Presentation of Product Manufa
cturing Information (PMI)---4.0---2014-10-13'),
/* implementation_level */ '2;1');

FILE_NAME(
/* name */ 'Socket Screw 7.step',
/* time_stamp */ '2026-10-24T18:52:33-07:00',
/* author */ (''),
/* organization */ (''),
/* preprocessor_version */ 'ST-DEVELOPER v20.2',
/* originating_system */ 'Autodesk Translation Framework v15.17.0.0',
/* authorisation */ '');

FILE_SCHEMA (('AP242_MANAGED_MODEL_BASED_3D_ENGINEERING_MIM_LF { 1 0 10303 442 2 1 4 }'));
ENDSEC;

DATA;
#10=MECHANICAL_DESIGN_GEOMETRIC_PRESENTATION_REPRESENTATION('',(#445),#34876);
#379=SHAPE_REPRESENTATION_RELATIONSHIP('SRR','None',#35016,#412);
#412=ADVANCED_BREP_SHAPE_REPRESENTATION('',(#478),#34874);
#445=STYLED_ITEM('',(#35159),#478);
#478=MANIFOLD_SOLID_BREP('Socket Screw 7',#19585);
#1065=PLANE('',#22148);
#1066=PLANE('',#22149);
#1067=PLANE('',#22153);
#1068=PLANE('',#22154);
#1069=PLANE('',#22155);
#1070=PLANE('',#22156);
#1071=PLANE('',#22157);
#1072=PLANE('',#22158);
#2649=LINE('',#34377,#4248);
#2650=LINE('',#34379,#4249);
#2651=LINE('',#34381,#4250);
#2652=LINE('',#34382,#4251);
#2653=LINE('',#34386,#4252);
#2654=LINE('',#34388,#4253);
#2655=LINE('',#34390,#4254);
#2656=LINE('',#34391,#4255);
#2657=LINE('',#34395,#4256);
#2658=LINE('',#34399,#4257);
#2659=LINE('',#34400,#4258);
#2660=LINE('',#34403,#4259);
#2661=LINE('',#34405,#4260);
#2662=LINE('',#34406,#4261);
#2663=LINE('',#34409,#4262);
#2664=LINE('',#34410,#4263);
#2665=LINE('',#34413,#4264);
#2666=LINE('',#34414,#4265);
#2667=LINE('',#34416,#4266);
#4248=VECTOR('',#28220,1.);
#4249=VECTOR('',#28221,1.);
#4250=VECTOR('',#28222,1.);
#4251=VECTOR('',#28223,1.);
#4252=VECTOR('',#28226,1.);
#4253=VECTOR('',#28227,1.);
#4254=VECTOR('',#28228,1.);
#4255=VECTOR('',#28229,1.);
#4256=VECTOR('',#28232,1.);
#4257=VECTOR('',#28239,1.);
#4258=VECTOR('',#28240,1.);
#4259=VECTOR('',#28243,1.);
#4260=VECTOR('',#28244,1.);
#4261=VECTOR('',#28245,1.);
#4262=VECTOR('',#28248,1.);
#4263=VECTOR('',#28249,1.);
#4264=VECTOR('',#28252,1.);
#4265=VECTOR('',#28253,1.);
#4266=VECTOR('',#28256,1.);
#4790=CYLINDRICAL_SURFACE('',#22150,0.0005);
#5799=FACE_OUTER_BOUND('',#6952,.T.);
#5800=FACE_OUTER_BOUND('',#6953,.T.);
#5801=FACE_OUTER_BOUND('',#6954,.T.);
#5802=FACE_OUTER_BOUND('',#6955,.T.);
#5803=FACE_OUTER_BOUND('',#6956,.T.);
#5804=FACE_OUTER_BOUND('',#6957,.T.);
#5805=FACE_OUTER_BOUND('',#6958,.T.);
#5806=FACE_OUTER_BOUND('',#6959,.T.);
#5807=FACE_OUTER_BOUND('',#6960,.T.);
#6952=EDGE_LOOP('',(#18298,#18299,#18300,#18301));
#6953=EDGE_LOOP('',(#18302,#18303,#18304,#18305));
#6954=EDGE_LOOP('',(#18306,#18307,#18308,#18309));
#6955=EDGE_LOOP('',(#18310,#18311,#18312,#18313));
#6956=EDGE_LOOP('',(#18314,#18315,#18316,#18317,#18318,#18319,#18320));
#6957=EDGE_LOOP('',(#18321,#18322,#18323,#18324));
#6958=EDGE_LOOP('',(#18325,#18326,#18327,#18328,#18329,#18330,#18331));
#6959=EDGE_LOOP('',(#18332,#18333,#18334,#18335));
#6960=EDGE_LOOP('',(#18336,#18337,#18338,#18339));
#8039=CIRCLE('',#22151,0.00050000000001);
#8040=CIRCLE('',#22152,0.00050000000001);
#9895=VERTEX_POINT('',#34375);
#9896=VERTEX_POINT('',#34376);
#9897=VERTEX_POINT('',#34378);
#9898=VERTEX_POINT('',#34380);
#9899=VERTEX_POINT('',#34384);
#9900=VERTEX_POINT('',#34385);
#9901=VERTEX_POINT('',#34387);
#9902=VERTEX_POINT('',#34389);
#9903=VERTEX_POINT('',#34393);
#9904=VERTEX_POINT('',#34394);
#9905=VERTEX_POINT('',#34402);
#9906=VERTEX_POINT('',#34404);
#9907=VERTEX_POINT('',#34408);
#9908=VERTEX_POINT('',#34412);
#12707=EDGE_CURVE('',#9895,#9896,#2649,.T.);
#12708=EDGE_CURVE('',#9896,#9897,#2650,.T.);
#12709=EDGE_CURVE('',#9897,#9898,#2651,.T.);
#12710=EDGE_CURVE('',#9895,#9898,#2652,.T.);
#12711=EDGE_CURVE('',#9899,#9900,#2653,.T.);
#12712=EDGE_CURVE('',#9899,#9901,#2654,.T.);
#12713=EDGE_CURVE('',#9901,#9902,#2655,.T.);
#12714=EDGE_CURVE('',#9900,#9902,#2656,.T.);
#12715=EDGE_CURVE('',#9903,#9904,#2657,.T.);
#12716=EDGE_CURVE('',#9903,#9899,#8039,.T.);
#12717=EDGE_CURVE('',#9904,#9900,#8040,.T.);
#12718=EDGE_CURVE('',#9902,#9897,#2658,.T.);
#12719=EDGE_CURVE('',#9898,#9901,#2659,.T.);
#12720=EDGE_CURVE('',#9905,#9896,#2660,.T.);
#12721=EDGE_CURVE('',#9906,#9905,#2661,.T.);
#12722=EDGE_CURVE('',#9904,#9906,#2662,.T.);
#12723=EDGE_CURVE('',#9907,#9906,#2663,.T.);
#12724=EDGE_CURVE('',#9903,#9907,#2664,.T.);
#12725=EDGE_CURVE('',#9908,#9907,#2665,.T.);
#12726=EDGE_CURVE('',#9895,#9908,#2666,.T.);
#12727=EDGE_CURVE('',#9905,#9908,#2667,.T.);
#18298=ORIENTED_EDGE('',*,*,#12707,.T.);
#18299=ORIENTED_EDGE('',*,*,#12708,.T.);
#18300=ORIENTED_EDGE('',*,*,#12709,.T.);
#18301=ORIENTED_EDGE('',*,*,#12710,.F.);
#18302=ORIENTED_EDGE('',*,*,#12711,.F.);
#18303=ORIENTED_EDGE('',*,*,#12712,.T.);
#18304=ORIENTED_EDGE('',*,*,#12713,.T.);
#18305=ORIENTED_EDGE('',*,*,#12714,.F.);
#18306=ORIENTED_EDGE('',*,*,#12715,.F.);
#18307=ORIENTED_EDGE('',*,*,#12716,.T.);
#18308=ORIENTED_EDGE('',*,*,#12711,.T.);
#18309=ORIENTED_EDGE('',*,*,#12717,.F.);
#18310=ORIENTED_EDGE('',*,*,#12709,.F.);
#18311=ORIENTED_EDGE('',*,*,#12718,.F.);
#18312=ORIENTED_EDGE('',*,*,#12713,.F.);
#18313=ORIENTED_EDGE('',*,*,#12719,.F.);
#18314=ORIENTED_EDGE('',*,*,#12720,.F.);
#18315=ORIENTED_EDGE('',*,*,#12721,.F.);
#18316=ORIENTED_EDGE('',*,*,#12722,.F.);
#18317=ORIENTED_EDGE('',*,*,#12717,.T.);
#18318=ORIENTED_EDGE('',*,*,#12714,.T.);
#18319=ORIENTED_EDGE('',*,*,#12718,.T.);
#18320=ORIENTED_EDGE('',*,*,#12708,.F.);
#18321=ORIENTED_EDGE('',*,*,#12722,.T.);
#18322=ORIENTED_EDGE('',*,*,#12723,.F.);
#18323=ORIENTED_EDGE('',*,*,#12724,.F.);
#18324=ORIENTED_EDGE('',*,*,#12715,.T.);
#18325=ORIENTED_EDGE('',*,*,#12724,.T.);
#18326=ORIENTED_EDGE('',*,*,#12725,.F.);
#18327=ORIENTED_EDGE('',*,*,#12726,.F.);
#18328=ORIENTED_EDGE('',*,*,#12710,.T.);
#18329=ORIENTED_EDGE('',*,*,#12719,.T.);
#18330=ORIENTED_EDGE('',*,*,#12712,.F.);
#18331=ORIENTED_EDGE('',*,*,#12716,.F.);
#18332=ORIENTED_EDGE('',*,*,#12726,.T.);
#18333=ORIENTED_EDGE('',*,*,#12727,.F.);
#18334=ORIENTED_EDGE('',*,*,#12720,.T.);
#18335=ORIENTED_EDGE('',*,*,#12707,.F.);
#18336=ORIENTED_EDGE('',*,*,#12727,.T.);
#18337=ORIENTED_EDGE('',*,*,#12725,.T.);
#18338=ORIENTED_EDGE('',*,*,#12723,.T.);
#18339=ORIENTED_EDGE('',*,*,#12721,.T.);
#19515=ADVANCED_FACE('',(#5799),#1065,.T.);
#19516=ADVANCED_FACE('',(#5800),#1066,.F.);
#19517=ADVANCED_FACE('',(#5801),#4790,.T.);
#19518=ADVANCED_FACE('',(#5802),#1067,.F.);
#19519=ADVANCED_FACE('',(#5803),#1068,.T.);
#19520=ADVANCED_FACE('',(#5804),#1069,.T.);
#19521=ADVANCED_FACE('',(#5805),#1070,.T.);
#19522=ADVANCED_FACE('',(#5806),#1071,.T.);
#19523=ADVANCED_FACE('',(#5807),#1072,.T.);
#19585=CLOSED_SHELL('',(#19515,#19516,#19517,#19518,#19519,#19520,#19521,
#19522,#19523));
#22147=AXIS2_PLACEMENT_3D('',#34373,#28216,#28217);
#22148=AXIS2_PLACEMENT_3D('',#34374,#28218,#28219);
#22149=AXIS2_PLACEMENT_3D('',#34383,#28224,#28225);
#22150=AXIS2_PLACEMENT_3D('',#34392,#28230,#28231);
#22151=AXIS2_PLACEMENT_3D('',#34396,#28233,#28234);
#22152=AXIS2_PLACEMENT_3D('',#34397,#28235,#28236);
#22153=AXIS2_PLACEMENT_3D('',#34398,#28237,#28238);
#22154=AXIS2_PLACEMENT_3D('',#34401,#28241,#28242);
#22155=AXIS2_PLACEMENT_3D('',#34407,#28246,#28247);
#22156=AXIS2_PLACEMENT_3D('',#34411,#28250,#28251);
#22157=AXIS2_PLACEMENT_3D('',#34415,#28254,#28255);
#22158=AXIS2_PLACEMENT_3D('',#34417,#28257,#28258);
#28216=DIRECTION('axis',(0.,0.,1.));
#28217=DIRECTION('refdir',(1.,0.,0.));
#28218=DIRECTION('center_axis',(1.,5.1420277733694E-16,-1.0522467400333E-14));
#28219=DIRECTION('ref_axis',(-1.0522467400333E-14,1.06077175752244E-14,
-1.));
#28220=DIRECTION('',(-1.00001914094642E-12,1.00002200370999E-12,1.));
#28221=DIRECTION('',(-9.47915311079142E-15,-1.,1.E-14));
#28222=DIRECTION('',(1.00001914094642E-12,-9.99999999998997E-13,-1.));
#28223=DIRECTION('',(-9.47915311079142E-15,-1.,1.E-14));
#28224=DIRECTION('center_axis',(1.,5.2084688920845E-16,-1.0522467400333E-14));
#28225=DIRECTION('ref_axis',(-1.0522467400333E-14,1.01548957588061E-14,
-1.));
#28226=DIRECTION('',(-9.56631913100564E-15,9.99999999999985E-15,1.));
#28227=DIRECTION('',(-9.47915311079142E-15,-1.,1.E-14));
#28228=DIRECTION('',(-9.56631913100564E-15,9.99999999999985E-15,1.));
#28229=DIRECTION('',(-9.47915311079142E-15,-1.,1.E-14));
#28230=DIRECTION('center_axis',(0.,-4.29362650667545E-31,1.));
#28231=DIRECTION('ref_axis',(4.28756753891971E-16,-1.,-4.29362650667545E-31));
#28232=DIRECTION('',(-9.99999999999976E-15,-1.04336808689941E-14,1.));
#28233=DIRECTION('center_axis',(-1.99999999991998E-11,2.E-11,1.));
#28234=DIRECTION('ref_axis',(-1.99995712428458E-11,-1.,1.99999999996E-11));
#28235=DIRECTION('center_axis',(-1.99999999991998E-11,2.E-11,1.));
#28236=DIRECTION('ref_axis',(-1.99995712428458E-11,-1.,1.99999999996E-11));
#28237=DIRECTION('center_axis',(-4.5961454925099E-16,1.,6.61092274672771E-17));
#28238=DIRECTION('ref_axis',(-1.05885766278003E-14,6.61092274672722E-17,
-1.));
#28239=DIRECTION('',(1.,-9.54038545074888E-15,9.9999999999998E-15));
#28240=DIRECTION('',(-1.,9.54038545074888E-15,-9.9999999999998E-15));
#28241=DIRECTION('center_axis',(-2.43331626335218E-16,4.46289580949563E-15,
1.));
#28242=DIRECTION('ref_axis',(1.,3.89820370584558E-15,2.43331626335201E-16));
#28243=DIRECTION('',(-1.,9.99485333130104E-13,-9.99628143109513E-13));
#28244=DIRECTION('',(-9.99479153109778E-13,-1.,1.0044628958085E-12));
#28245=DIRECTION('',(1.,-9.99466108488984E-13,1.00024333162532E-12));
#28246=DIRECTION('center_axis',(-5.3389151001178E-16,1.,6.61092274672815E-17));
#28247=DIRECTION('ref_axis',(-9.50035731417012E-15,6.61092274672764E-17,
-1.));
#28248=DIRECTION('',(-9.99999999998985E-13,-1.00108821931263E-12,1.));
#28249=DIRECTION('',(1.,-9.99466108488984E-13,1.00024333162532E-12));
#28250=DIRECTION('center_axis',(-1.0522467400333E-14,-4.46289580949556E-15,
-1.));
#28251=DIRECTION('ref_axis',(1.,-6.86759532082262E-15,-1.0522467400333E-14));
#28252=DIRECTION('',(9.99479153109778E-13,1.,-1.0044628958085E-12));
#28253=DIRECTION('',(1.,-9.99466108488984E-13,1.00024333162532E-12));
#28254=DIRECTION('center_axis',(5.33891510011771E-16,-1.,2.20037109950003E-17));
#28255=DIRECTION('ref_axis',(-1.,-5.33891510011771E-16,1.0522467400333E-14));
#28256=DIRECTION('',(9.99999999998993E-13,-1.00002200370999E-12,-1.));
#28257=DIRECTION('center_axis',(1.,5.33891510011885E-16,-1.0522467400333E-14));
#28258=DIRECTION('ref_axis',(-1.0522467400333E-14,1.08319082541355E-14,
-1.));
#34373=CARTESIAN_POINT('',(0.,0.,0.));
#34374=CARTESIAN_POINT('Origin',(0.02115,-0.0223,-0.01175));
#34375=CARTESIAN_POINT('',(0.02115,-0.02545,-0.00125000000000007));
#34376=CARTESIAN_POINT('',(0.02115,-0.02545,-0.000750000000000074));
#34377=CARTESIAN_POINT('',(0.02115000000001,-0.02545000000001,-0.00649999999999003));
#34378=CARTESIAN_POINT('',(0.02115,-0.0317,-0.000750000000000074));
#34379=CARTESIAN_POINT('',(0.0211500000000101,-0.02545000000001,-0.000749999999990073));
#34380=CARTESIAN_POINT('',(0.02115,-0.0317,-0.00125000000000007));
#34381=CARTESIAN_POINT('',(0.0211500000000101,-0.0317000000000099,-0.00549999999999003));
#34382=CARTESIAN_POINT('',(0.0211500000000101,-0.02545000000001,-0.00124999999999007));
#34383=CARTESIAN_POINT('Origin',(0.02065,-0.02545,-0.000750000000000068));
#34384=CARTESIAN_POINT('',(0.02065,-0.02545,-0.00125000000000007));
#34385=CARTESIAN_POINT('',(0.02065,-0.02545,-0.000750000000000068));
#34386=CARTESIAN_POINT('',(0.0206500000000101,-0.02545000000001,-0.000749999999990068));
#34387=CARTESIAN_POINT('',(0.02065,-0.0317,-0.00125000000000007));
#34388=CARTESIAN_POINT('',(0.0206500000000101,-0.02545000000001,-0.00124999999999007));
#34389=CARTESIAN_POINT('',(0.02065,-0.0317,-0.000750000000000068));
#34390=CARTESIAN_POINT('',(0.0206500000000101,-0.03170000000001,-0.000749999999990068));
#34391=CARTESIAN_POINT('',(0.0206500000000101,-0.02545000000001,-0.000749999999990068));
#34392=CARTESIAN_POINT('Origin',(0.02115,-0.02545,-0.00100000000000007));
#34393=CARTESIAN_POINT('',(0.02115,-0.02495,-0.00125000000000007));
#34394=CARTESIAN_POINT('',(0.02115,-0.02495,-0.000750000000000074));
#34395=CARTESIAN_POINT('',(0.0211500000000101,-0.02495000000001,-0.000749999999990073));
#34396=CARTESIAN_POINT('Origin',(0.0211500000000101,-0.02545000000001,-0.00124999999999007));
#34397=CARTESIAN_POINT('Origin',(0.0211500000000101,-0.02545000000001,-0.000749999999990073));
#34398=CARTESIAN_POINT('Origin',(0.02115,-0.0317,0.000749999999999928));
#34399=CARTESIAN_POINT('',(0.0206500000000101,-0.03170000000001,-0.000749999999990068));
#34400=CARTESIAN_POINT('',(0.0206500000000101,-0.03170000000001,-0.00124999999999007));
#34401=CARTESIAN_POINT('Origin',(0.0229,-0.02495,-0.000750000000000093));
#34402=CARTESIAN_POINT('',(0.0262,-0.02545,-0.000750000000000127));
#34403=CARTESIAN_POINT('',(0.0229000000000101,-0.02545000000001,-0.000749999999990092));
#34404=CARTESIAN_POINT('',(0.0262,-0.02495,-0.000750000000000127));
#34405=CARTESIAN_POINT('',(0.0262000000000101,-0.02545000000001,-0.000749999999990028));
#34406=CARTESIAN_POINT('',(0.0229000000000101,-0.02495000000001,-0.000749999999990092));
#34407=CARTESIAN_POINT('Origin',(0.0229,-0.02495,-0.00125000000000009));
#34408=CARTESIAN_POINT('',(0.0262,-0.02495,-0.00125000000000013));
#34409=CARTESIAN_POINT('',(0.0262000000000101,-0.02495000000001,-0.000749999999990028));
#34410=CARTESIAN_POINT('',(0.0229000000000101,-0.02495000000001,-0.00124999999999009));
#34411=CARTESIAN_POINT('Origin',(0.0229,-0.02545,-0.00125000000000009));
#34412=CARTESIAN_POINT('',(0.0262,-0.02545,-0.00125000000000013));
#34413=CARTESIAN_POINT('',(0.0262000000000102,-0.02495000000001,-0.00124999999999003));
#34414=CARTESIAN_POINT('',(0.0229000000000101,-0.02545000000001,-0.00124999999999009));
#34415=CARTESIAN_POINT('Origin',(0.0229,-0.02545,-0.000750000000000093));
#34416=CARTESIAN_POINT('',(0.0262000000000102,-0.02545000000001,-0.00124999999999003));
#34417=CARTESIAN_POINT('Origin',(0.0262,-0.0252,-0.00100000000000013));
#34839=UNCERTAINTY_MEASURE_WITH_UNIT(LENGTH_MEASURE(1.E-5),#34877,
'DISTANCE_ACCURACY_VALUE',
'Maximum model space distance between geometric entities at asserted c
onnectivities');
#34841=UNCERTAINTY_MEASURE_WITH_UNIT(LENGTH_MEASURE(1.E-5),#34877,
'DISTANCE_ACCURACY_VALUE',
'Maximum model space distance between geometric entities at asserted c
onnectivities');
#34874=(
GEOMETRIC_REPRESENTATION_CONTEXT(3)
GLOBAL_UNCERTAINTY_ASSIGNED_CONTEXT((#34839))
GLOBAL_UNIT_ASSIGNED_CONTEXT((#34877,#34878,#34879))
REPRESENTATION_CONTEXT('','3D')
);
#34876=(
GEOMETRIC_REPRESENTATION_CONTEXT(3)
GLOBAL_UNCERTAINTY_ASSIGNED_CONTEXT((#34841))
GLOBAL_UNIT_ASSIGNED_CONTEXT((#34877,#34878,#34879))
REPRESENTATION_CONTEXT('','3D')
);
#34877=(
LENGTH_UNIT()
NAMED_UNIT(*)
SI_UNIT($,.METRE.)
);
#34878=(
NAMED_UNIT(*)
PLANE_ANGLE_UNIT()
SI_UNIT($,.RADIAN.)
);
#34879=(
NAMED_UNIT(*)
SI_UNIT($,.STERADIAN.)
SOLID_ANGLE_UNIT()
);
#34912=SHAPE_DEFINITION_REPRESENTATION(#34946,#35016);
#34946=PRODUCT_DEFINITION_SHAPE('',$,#35051);
#35016=SHAPE_REPRESENTATION('',(#22147),#34874);
#35018=PRODUCT_DEFINITION_CONTEXT('part definition',#35122,'design');
#35051=PRODUCT_DEFINITION('Socket Screw 7','Socket Screw 7',#35085,#35018);
#35085=PRODUCT_DEFINITION_FORMATION('',$,#35156);
#35122=APPLICATION_CONTEXT('Managed model based 3d engineering');
#35123=PRODUCT_CONTEXT('part definition',#35122,'mechanical');
#35156=PRODUCT('Socket Screw 7','Socket Screw 7',
'LEGAL AND USAGE DISCLAIMER: this Data/Model is provided \X2\201C\X0\A
S IS\X2\201D\X0\ for informational and representational only. It is a 
geometric approximation and is NOT engineered, certified, or guarantee
d for dimensional accuracy, exact tolerances, or production-level prec
ision. Vendor disclaims all implied warranties including fitness for a
 particular purpose. DO NOT USE FOR DIRECT PHYSICAL MANUFACTURING, AUT
OMATED PRODUCTION, OR SAFETY-CRITICAL SYSTEMS without independent engi
neering verification and resolution of any design discrepancies.',(#35123));
#35159=PRESENTATION_STYLE_ASSIGNMENT((#35168));
#35168=SURFACE_STYLE_USAGE(.BOTH.,#35177);
#35177=SURFACE_SIDE_STYLE('',(#35186));
#35186=SURFACE_STYLE_FILL_AREA(#35195);
#35195=FILL_AREA_STYLE('Paint - Enamel Glossy (White)',(#35204));
#35204=FILL_AREA_STYLE_COLOUR('Paint - Enamel Glossy (White)',#35213);
#35213=COLOUR_RGB('Paint - Enamel Glossy (White)',0.964705882352941,0.964705882352941,
0.952941176470588);
ENDSEC;
END-ISO-10303-21;
